ISO-10303-21;
HEADER;
/* Generated by software containing ST-Developer
 * from STEP Tools, Inc. (www.steptools.com) 
 */

FILE_DESCRIPTION(
/* description */ ('Drill jig with bushing plate'),
/* implementation_level */ '2;1');

FILE_NAME(
/* name */ 'Hinge lug (1).step',
/* time_stamp */ '2026-10-27T10:51:08-07:00',
/* author */ (''),
/* organization */ (''),
/* preprocessor_version */ 'ST-DEVELOPER v20.2',
/* originating_system */ 'Autodesk Translation Framework v15.17.0.0',
/* authorisation */ '');

FILE_SCHEMA (('AUTOMOTIVE_DESIGN { 1 0 10303 214 3 1 1 }'));
ENDSEC;

DATA;
#10=MECHANICAL_DESIGN_GEOMETRIC_PRESENTATION_REPRESENTATION('',(#231),#6638);
#174=B_SPLINE_CURVE_WITH_KNOTS('',3,(#5889,#5890,#5891,#5892,#5893,#5894,
#5895,#5896,#5897,#5898,#5899,#5900,#5901,#5902,#5903,#5904,#5905,#5906,
#5907,#5908,#5909,#5910,#5911,#5912,#5913,#5914,#5915,#5916,#5917,#5918,
#5919,#5920,#5921,#5922,#5923,#5924,#5925,#5926,#5927,#5928,#5929,#5930,
#5931,#5932,#5933,#5934,#5935,#5936,#5937,#5938),.UNSPECIFIED.,.T.,.F.,
(4,2,2,2,2,2,2,2,2,2,2,2,2,2,2,2,2,2,2,2,2,2,2,2,4),(0.,0.177519856988816,
0.355039713977633,0.436196019741432,0.517352325505232,0.678532215702782,
0.839712105900332,1.00089199609788,1.16207188629543,1.24322819205923,1.32438449782303,
1.50190435481185,1.67942421180066,1.85694406878948,2.0344639257783,2.1156202315421,
2.1967765373059,2.35795642750345,2.519136317701,2.68031620789855,2.8414960980961,
2.9226524038599,3.0038087096237,3.18132856661251,3.35884842360133),
 .UNSPECIFIED.);
#183=SHAPE_REPRESENTATION_RELATIONSHIP('SRR','None',#6747,#207);
#207=ADVANCED_BREP_SHAPE_REPRESENTATION('',(#255),#6620);
#231=STYLED_ITEM('',(#6957),#255);
#255=MANIFOLD_SOLID_BREP('Body1',#3598);
#319=FACE_BOUND('',#840,.T.);
#320=FACE_BOUND('',#842,.T.);
#321=FACE_BOUND('',#846,.T.);
#322=FACE_BOUND('',#848,.T.);
#323=FACE_BOUND('',#851,.T.);
#324=FACE_BOUND('',#854,.T.);
#325=FACE_BOUND('',#855,.T.);
#326=FACE_BOUND('',#858,.T.);
#327=FACE_BOUND('',#860,.T.);
#414=PLANE('',#4029);
#415=PLANE('',#4039);
#416=PLANE('',#4040);
#417=PLANE('',#4041);
#418=PLANE('',#4042);
#419=PLANE('',#4043);
#420=PLANE('',#4044);
#421=PLANE('',#4045);
#422=PLANE('',#4046);
#575=FACE_OUTER_BOUND('',#839,.T.);
#576=FACE_OUTER_BOUND('',#841,.T.);
#577=FACE_OUTER_BOUND('',#843,.T.);
#578=FACE_OUTER_BOUND('',#844,.T.);
#579=FACE_OUTER_BOUND('',#845,.T.);
#580=FACE_OUTER_BOUND('',#847,.T.);
#581=FACE_OUTER_BOUND('',#849,.T.);
#582=FACE_OUTER_BOUND('',#850,.T.);
#583=FACE_OUTER_BOUND('',#852,.T.);
#584=FACE_OUTER_BOUND('',#853,.T.);
#585=FACE_OUTER_BOUND('',#856,.T.);
#586=FACE_OUTER_BOUND('',#857,.T.);
#587=FACE_OUTER_BOUND('',#859,.T.);
#839=EDGE_LOOP('',(#2751,#2752,#2753,#2754));
#840=EDGE_LOOP('',(#2755));
#841=EDGE_LOOP('',(#2756));
#842=EDGE_LOOP('',(#2757));
#843=EDGE_LOOP('',(#2758,#2759,#2760,#2761));
#844=EDGE_LOOP('',(#2762,#2763,#2764,#2765));
#845=EDGE_LOOP('',(#2766,#2767,#2768,#2769));
#846=EDGE_LOOP('',(#2770));
#847=EDGE_LOOP('',(#2771,#2772,#2773,#2774));
#848=EDGE_LOOP('',(#2775));
#849=EDGE_LOOP('',(#2776,#2777,#2778,#2779));
#850=EDGE_LOOP('',(#2780,#2781,#2782,#2783));
#851=EDGE_LOOP('',(#2784));
#852=EDGE_LOOP('',(#2785,#2786,#2787,#2788));
#853=EDGE_LOOP('',(#2789,#2790,#2791,#2792));
#854=EDGE_LOOP('',(#2793));
#855=EDGE_LOOP('',(#2794));
#856=EDGE_LOOP('',(#2795,#2796,#2797,#2798));
#857=EDGE_LOOP('',(#2799,#2800,#2801,#2802,#2803,#2804));
#858=EDGE_LOOP('',(#2805));
#859=EDGE_LOOP('',(#2806,#2807,#2808,#2809,#2810,#2811));
#860=EDGE_LOOP('',(#2812));
#1126=LINE('',#5886,#1387);
#1127=LINE('',#5945,#1388);
#1128=LINE('',#5950,#1389);
#1129=LINE('',#5956,#1390);
#1130=LINE('',#5961,#1391);
#1131=LINE('',#5963,#1392);
#1132=LINE('',#5965,#1393);
#1133=LINE('',#5966,#1394);
#1134=LINE('',#5969,#1395);
#1135=LINE('',#5971,#1396);
#1136=LINE('',#5972,#1397);
#1137=LINE('',#5975,#1398);
#1138=LINE('',#5977,#1399);
#1139=LINE('',#5978,#1400);
#1140=LINE('',#5981,#1401);
#1141=LINE('',#5983,#1402);
#1142=LINE('',#5984,#1403);
#1143=LINE('',#5987,#1404);
#1144=LINE('',#5989,#1405);
#1145=LINE('',#5990,#1406);
#1146=LINE('',#5992,#1407);
#1147=LINE('',#5993,#1408);
#1387=VECTOR('',#4719,0.475);
#1388=VECTOR('',#4730,0.275);
#1389=VECTOR('',#4735,0.275);
#1390=VECTOR('',#4742,0.405);
#1391=VECTOR('',#4747,1.);
#1392=VECTOR('',#4748,1.);
#1393=VECTOR('',#4749,1.);
#1394=VECTOR('',#4750,1.);
#1395=VECTOR('',#4753,1.);
#1396=VECTOR('',#4754,1.);
#1397=VECTOR('',#4755,1.);
#1398=VECTOR('',#4758,1.);
#1399=VECTOR('',#4759,1.);
#1400=VECTOR('',#4760,1.);
#1401=VECTOR('',#4763,1.);
#1402=VECTOR('',#4764,1.);
#1403=VECTOR('',#4765,1.);
#1404=VECTOR('',#4768,1.);
#1405=VECTOR('',#4769,1.);
#1406=VECTOR('',#4770,1.);
#1407=VECTOR('',#4773,1.);
#1408=VECTOR('',#4774,1.);
#1612=CIRCLE('',#4027,0.475);
#1613=CIRCLE('',#4028,0.475);
#1614=CIRCLE('',#4030,0.275);
#1615=CIRCLE('',#4032,0.275);
#1616=CIRCLE('',#4034,0.275);
#1617=CIRCLE('',#4035,0.275);
#1618=CIRCLE('',#4037,0.405);
#1619=CIRCLE('',#4038,0.405);
#1825=VERTEX_POINT('',#5883);
#1826=VERTEX_POINT('',#5885);
#1827=VERTEX_POINT('',#5888);
#1828=VERTEX_POINT('',#5940);
#1829=VERTEX_POINT('',#5943);
#1830=VERTEX_POINT('',#5947);
#1831=VERTEX_POINT('',#5949);
#1832=VERTEX_POINT('',#5953);
#1833=VERTEX_POINT('',#5955);
#1834=VERTEX_POINT('',#5959);
#1835=VERTEX_POINT('',#5960);
#1836=VERTEX_POINT('',#5962);
#1837=VERTEX_POINT('',#5964);
#1838=VERTEX_POINT('',#5968);
#1839=VERTEX_POINT('',#5970);
#1840=VERTEX_POINT('',#5974);
#1841=VERTEX_POINT('',#5976);
#1842=VERTEX_POINT('',#5980);
#1843=VERTEX_POINT('',#5982);
#1844=VERTEX_POINT('',#5986);
#1845=VERTEX_POINT('',#5988);
#2163=EDGE_CURVE('',#1825,#1825,#1612,.T.);
#2164=EDGE_CURVE('',#1825,#1826,#1126,.T.);
#2165=EDGE_CURVE('',#1826,#1826,#1613,.T.);
#2166=EDGE_CURVE('',#1827,#1827,#174,.T.);
#2167=EDGE_CURVE('',#1828,#1828,#1614,.T.);
#2168=EDGE_CURVE('',#1829,#1829,#1615,.T.);
#2169=EDGE_CURVE('',#1829,#1828,#1127,.T.);
#2170=EDGE_CURVE('',#1830,#1830,#1616,.T.);
#2171=EDGE_CURVE('',#1830,#1831,#1128,.T.);
#2172=EDGE_CURVE('',#1831,#1831,#1617,.T.);
#2173=EDGE_CURVE('',#1832,#1832,#1618,.T.);
#2174=EDGE_CURVE('',#1832,#1833,#1129,.T.);
#2175=EDGE_CURVE('',#1833,#1833,#1619,.T.);
#2176=EDGE_CURVE('',#1834,#1835,#1130,.T.);
#2177=EDGE_CURVE('',#1835,#1836,#1131,.T.);
#2178=EDGE_CURVE('',#1837,#1836,#1132,.T.);
#2179=EDGE_CURVE('',#1834,#1837,#1133,.T.);
#2180=EDGE_CURVE('',#1838,#1834,#1134,.T.);
#2181=EDGE_CURVE('',#1839,#1837,#1135,.T.);
#2182=EDGE_CURVE('',#1838,#1839,#1136,.T.);
#2183=EDGE_CURVE('',#1840,#1838,#1137,.T.);
#2184=EDGE_CURVE('',#1841,#1839,#1138,.T.);
#2185=EDGE_CURVE('',#1840,#1841,#1139,.T.);
#2186=EDGE_CURVE('',#1842,#1840,#1140,.T.);
#2187=EDGE_CURVE('',#1843,#1841,#1141,.T.);
#2188=EDGE_CURVE('',#1842,#1843,#1142,.T.);
#2189=EDGE_CURVE('',#1844,#1842,#1143,.T.);
#2190=EDGE_CURVE('',#1845,#1843,#1144,.T.);
#2191=EDGE_CURVE('',#1844,#1845,#1145,.T.);
#2192=EDGE_CURVE('',#1835,#1844,#1146,.T.);
#2193=EDGE_CURVE('',#1836,#1845,#1147,.T.);
#2751=ORIENTED_EDGE('',*,*,#2163,.F.);
#2752=ORIENTED_EDGE('',*,*,#2164,.T.);
#2753=ORIENTED_EDGE('',*,*,#2165,.F.);
#2754=ORIENTED_EDGE('',*,*,#2164,.F.);
#2755=ORIENTED_EDGE('',*,*,#2166,.F.);
#2756=ORIENTED_EDGE('',*,*,#2163,.T.);
#2757=ORIENTED_EDGE('',*,*,#2167,.F.);
#2758=ORIENTED_EDGE('',*,*,#2168,.F.);
#2759=ORIENTED_EDGE('',*,*,#2169,.T.);
#2760=ORIENTED_EDGE('',*,*,#2167,.T.);
#2761=ORIENTED_EDGE('',*,*,#2169,.F.);
#2762=ORIENTED_EDGE('',*,*,#2170,.F.);
#2763=ORIENTED_EDGE('',*,*,#2171,.T.);
#2764=ORIENTED_EDGE('',*,*,#2172,.F.);
#2765=ORIENTED_EDGE('',*,*,#2171,.F.);
#2766=ORIENTED_EDGE('',*,*,#2173,.F.);
#2767=ORIENTED_EDGE('',*,*,#2174,.T.);
#2768=ORIENTED_EDGE('',*,*,#2175,.F.);
#2769=ORIENTED_EDGE('',*,*,#2174,.F.);
#2770=ORIENTED_EDGE('',*,*,#2166,.T.);
#2771=ORIENTED_EDGE('',*,*,#2176,.T.);
#2772=ORIENTED_EDGE('',*,*,#2177,.T.);
#2773=ORIENTED_EDGE('',*,*,#2178,.F.);
#2774=ORIENTED_EDGE('',*,*,#2179,.F.);
#2775=ORIENTED_EDGE('',*,*,#2165,.T.);
#2776=ORIENTED_EDGE('',*,*,#2180,.T.);
#2777=ORIENTED_EDGE('',*,*,#2179,.T.);
#2778=ORIENTED_EDGE('',*,*,#2181,.F.);
#2779=ORIENTED_EDGE('',*,*,#2182,.F.);
#2780=ORIENTED_EDGE('',*,*,#2183,.T.);
#2781=ORIENTED_EDGE('',*,*,#2182,.T.);
#2782=ORIENTED_EDGE('',*,*,#2184,.F.);
#2783=ORIENTED_EDGE('',*,*,#2185,.F.);
#2784=ORIENTED_EDGE('',*,*,#2172,.T.);
#2785=ORIENTED_EDGE('',*,*,#2186,.T.);
#2786=ORIENTED_EDGE('',*,*,#2185,.T.);
#2787=ORIENTED_EDGE('',*,*,#2187,.F.);
#2788=ORIENTED_EDGE('',*,*,#2188,.F.);
#2789=ORIENTED_EDGE('',*,*,#2189,.T.);
#2790=ORIENTED_EDGE('',*,*,#2188,.T.);
#2791=ORIENTED_EDGE('',*,*,#2190,.F.);
#2792=ORIENTED_EDGE('',*,*,#2191,.F.);
#2793=ORIENTED_EDGE('',*,*,#2168,.T.);
#2794=ORIENTED_EDGE('',*,*,#2170,.T.);
#2795=ORIENTED_EDGE('',*,*,#2192,.T.);
#2796=ORIENTED_EDGE('',*,*,#2191,.T.);
#2797=ORIENTED_EDGE('',*,*,#2193,.F.);
#2798=ORIENTED_EDGE('',*,*,#2177,.F.);
#2799=ORIENTED_EDGE('',*,*,#2193,.T.);
#2800=ORIENTED_EDGE('',*,*,#2190,.T.);
#2801=ORIENTED_EDGE('',*,*,#2187,.T.);
#2802=ORIENTED_EDGE('',*,*,#2184,.T.);
#2803=ORIENTED_EDGE('',*,*,#2181,.T.);
#2804=ORIENTED_EDGE('',*,*,#2178,.T.);
#2805=ORIENTED_EDGE('',*,*,#2175,.T.);
#2806=ORIENTED_EDGE('',*,*,#2192,.F.);
#2807=ORIENTED_EDGE('',*,*,#2176,.F.);
#2808=ORIENTED_EDGE('',*,*,#2180,.F.);
#2809=ORIENTED_EDGE('',*,*,#2183,.F.);
#2810=ORIENTED_EDGE('',*,*,#2186,.F.);
#2811=ORIENTED_EDGE('',*,*,#2189,.F.);
#2812=ORIENTED_EDGE('',*,*,#2173,.T.);
#3329=CYLINDRICAL_SURFACE('',#4026,0.475);
#3330=CYLINDRICAL_SURFACE('',#4031,0.275);
#3331=CYLINDRICAL_SURFACE('',#4033,0.275);
#3332=CYLINDRICAL_SURFACE('',#4036,0.405);
#3450=ADVANCED_FACE('',(#575,#319),#3329,.F.);
#3451=ADVANCED_FACE('',(#576,#320),#414,.T.);
#3452=ADVANCED_FACE('',(#577),#3330,.F.);
#3453=ADVANCED_FACE('',(#578),#3331,.F.);
#3454=ADVANCED_FACE('',(#579,#321),#3332,.F.);
#3455=ADVANCED_FACE('',(#580,#322),#415,.T.);
#3456=ADVANCED_FACE('',(#581),#416,.T.);
#3457=ADVANCED_FACE('',(#582,#323),#417,.T.);
#3458=ADVANCED_FACE('',(#583),#418,.T.);
#3459=ADVANCED_FACE('',(#584,#324,#325),#419,.T.);
#3460=ADVANCED_FACE('',(#585),#420,.T.);
#3461=ADVANCED_FACE('',(#586,#326),#421,.T.);
#3462=ADVANCED_FACE('',(#587,#327),#422,.F.);
#3598=CLOSED_SHELL('',(#3450,#3451,#3452,#3453,#3454,#3455,#3456,#3457,
#3458,#3459,#3460,#3461,#3462));
#4025=AXIS2_PLACEMENT_3D('',#5881,#4713,#4714);
#4026=AXIS2_PLACEMENT_3D('',#5882,#4715,#4716);
#4027=AXIS2_PLACEMENT_3D('',#5884,#4717,#4718);
#4028=AXIS2_PLACEMENT_3D('',#5887,#4720,#4721);
#4029=AXIS2_PLACEMENT_3D('',#5939,#4722,#4723);
#4030=AXIS2_PLACEMENT_3D('',#5941,#4724,#4725);
#4031=AXIS2_PLACEMENT_3D('',#5942,#4726,#4727);
#4032=AXIS2_PLACEMENT_3D('',#5944,#4728,#4729);
#4033=AXIS2_PLACEMENT_3D('',#5946,#4731,#4732);
#4034=AXIS2_PLACEMENT_3D('',#5948,#4733,#4734);
#4035=AXIS2_PLACEMENT_3D('',#5951,#4736,#4737);
#4036=AXIS2_PLACEMENT_3D('',#5952,#4738,#4739);
#4037=AXIS2_PLACEMENT_3D('',#5954,#4740,#4741);
#4038=AXIS2_PLACEMENT_3D('',#5957,#4743,#4744);
#4039=AXIS2_PLACEMENT_3D('',#5958,#4745,#4746);
#4040=AXIS2_PLACEMENT_3D('',#5967,#4751,#4752);
#4041=AXIS2_PLACEMENT_3D('',#5973,#4756,#4757);
#4042=AXIS2_PLACEMENT_3D('',#5979,#4761,#4762);
#4043=AXIS2_PLACEMENT_3D('',#5985,#4766,#4767);
#4044=AXIS2_PLACEMENT_3D('',#5991,#4771,#4772);
#4045=AXIS2_PLACEMENT_3D('',#5994,#4775,#4776);
#4046=AXIS2_PLACEMENT_3D('',#5995,#4777,#4778);
#4713=DIRECTION('axis',(0.,0.,1.));
#4714=DIRECTION('refdir',(1.,0.,0.));
#4715=DIRECTION('center_axis',(0.,0.,1.));
#4716=DIRECTION('ref_axis',(1.,0.,0.));
#4717=DIRECTION('center_axis',(0.,0.,1.));
#4718=DIRECTION('ref_axis',(1.,0.,0.));
#4719=DIRECTION('',(0.,0.,1.));
#4720=DIRECTION('center_axis',(0.,0.,-1.));
#4721=DIRECTION('ref_axis',(1.,0.,0.));
#4722=DIRECTION('center_axis',(0.,0.,1.));
#4723=DIRECTION('ref_axis',(1.,0.,0.));
#4724=DIRECTION('center_axis',(0.,0.,1.));
#4725=DIRECTION('ref_axis',(1.,0.,0.));
#4726=DIRECTION('center_axis',(0.,0.,1.));
#4727=DIRECTION('ref_axis',(1.,0.,0.));
#4728=DIRECTION('center_axis',(0.,0.,1.));
#4729=DIRECTION('ref_axis',(1.,0.,0.));
#4730=DIRECTION('',(0.,0.,1.));
#4731=DIRECTION('center_axis',(0.,0.,1.));
#4732=DIRECTION('ref_axis',(1.,0.,0.));
#4733=DIRECTION('center_axis',(0.,0.,1.));
#4734=DIRECTION('ref_axis',(1.,0.,0.));
#4735=DIRECTION('',(0.,0.,1.));
#4736=DIRECTION('center_axis',(0.,0.,-1.));
#4737=DIRECTION('ref_axis',(1.,0.,0.));
#4738=DIRECTION('center_axis',(1.,0.,0.));
#4739=DIRECTION('ref_axis',(0.,0.,-1.));
#4740=DIRECTION('center_axis',(1.,0.,0.));
#4741=DIRECTION('ref_axis',(0.,0.,-1.));
#4742=DIRECTION('',(1.,0.,0.));
#4743=DIRECTION('center_axis',(-1.,0.,0.));
#4744=DIRECTION('ref_axis',(0.,0.,-1.));
#4745=DIRECTION('center_axis',(0.,0.,1.));
#4746=DIRECTION('ref_axis',(0.,-1.,0.));
#4747=DIRECTION('',(0.,-1.,0.));
#4748=DIRECTION('',(1.,0.,0.));
#4749=DIRECTION('',(0.,-1.,0.));
#4750=DIRECTION('',(1.,0.,0.));
#4751=DIRECTION('center_axis',(0.,1.,0.));
#4752=DIRECTION('ref_axis',(0.,0.,1.));
#4753=DIRECTION('',(0.,0.,1.));
#4754=DIRECTION('',(0.,0.,1.));
#4755=DIRECTION('',(1.,0.,0.));
#4756=DIRECTION('center_axis',(0.,0.,1.));
#4757=DIRECTION('ref_axis',(0.,-1.,0.));
#4758=DIRECTION('',(0.,-1.,0.));
#4759=DIRECTION('',(0.,-1.,0.));
#4760=DIRECTION('',(1.,0.,0.));
#4761=DIRECTION('center_axis',(0.,1.,0.));
#4762=DIRECTION('ref_axis',(0.,0.,1.));
#4763=DIRECTION('',(0.,0.,1.));
#4764=DIRECTION('',(0.,0.,1.));
#4765=DIRECTION('',(1.,0.,0.));
#4766=DIRECTION('center_axis',(0.,0.,-1.));
#4767=DIRECTION('ref_axis',(0.,1.,0.));
#4768=DIRECTION('',(0.,1.,0.));
#4769=DIRECTION('',(0.,1.,0.));
#4770=DIRECTION('',(1.,0.,0.));
#4771=DIRECTION('center_axis',(0.,-1.,0.));
#4772=DIRECTION('ref_axis',(0.,0.,-1.));
#4773=DIRECTION('',(0.,0.,-1.));
#4774=DIRECTION('',(0.,0.,-1.));
#4775=DIRECTION('center_axis',(1.,0.,0.));
#4776=DIRECTION('ref_axis',(0.,0.,-1.));
#4777=DIRECTION('center_axis',(1.,0.,0.));
#4778=DIRECTION('ref_axis',(0.,0.,-1.));
#5881=CARTESIAN_POINT('',(0.,0.,0.));
#5882=CARTESIAN_POINT('Origin',(6.5,-6.5,1.8));
#5883=CARTESIAN_POINT('',(6.025,-6.5,1.8));
#5884=CARTESIAN_POINT('Origin',(6.5,-6.5,1.8));
#5885=CARTESIAN_POINT('',(6.025,-6.5,4.5));
#5886=CARTESIAN_POINT('',(6.025,-6.5,1.8));
#5887=CARTESIAN_POINT('Origin',(6.5,-6.5,4.5));
#5888=CARTESIAN_POINT('',(6.0345969488712,-6.405,3.5));
#5889=CARTESIAN_POINT('Ctrl Pts',(6.0345969488712,-6.405,3.5));
#5890=CARTESIAN_POINT('Ctrl Pts',(6.0345969488712,-6.405,3.44082671433706));
#5891=CARTESIAN_POINT('Ctrl Pts',(6.03680805489022,-6.391162819218,3.3786038562345));
#5892=CARTESIAN_POINT('Ctrl Pts',(6.0525995429062,-6.33805779261652,3.26878119899199));
#5893=CARTESIAN_POINT('Ctrl Pts',(6.06703236747091,-6.29875591394082,3.22132213181236));
#5894=CARTESIAN_POINT('Ctrl Pts',(6.10302255777628,-6.23823300006139,3.17155768103299));
#5895=CARTESIAN_POINT('Ctrl Pts',(6.11762591851161,-6.2169021926909,3.15715697182391));
#5896=CARTESIAN_POINT('Ctrl Pts',(6.15217680980098,-6.17538739566531,3.13417605500228));
#5897=CARTESIAN_POINT('Ctrl Pts',(6.1721530169738,-6.1552757719279,3.12550838237099));
#5898=CARTESIAN_POINT('Ctrl Pts',(6.23204377410763,-6.10432382827604,3.1070097286502));
#5899=CARTESIAN_POINT('Ctrl Pts',(6.28153129405636,-6.07437258197005,3.10138466314703));
#5900=CARTESIAN_POINT('Ctrl Pts',(6.38865927826313,-6.03471454832095,3.09599463066268));
#5901=CARTESIAN_POINT('Ctrl Pts',(6.44627336993415,-6.025,3.09577234137185));
#5902=CARTESIAN_POINT('Ctrl Pts',(6.55372663006585,-6.025,3.09577234137185));
#5903=CARTESIAN_POINT('Ctrl Pts',(6.61134072173687,-6.03471454832095,3.09599463066268));
#5904=CARTESIAN_POINT('Ctrl Pts',(6.71846870594365,-6.07437258197005,3.10138466314703));
#5905=CARTESIAN_POINT('Ctrl Pts',(6.76795622589237,-6.10432382827604,3.1070097286502));
#5906=CARTESIAN_POINT('Ctrl Pts',(6.8278469830262,-6.1552757719279,3.12550838237099));
#5907=CARTESIAN_POINT('Ctrl Pts',(6.84782319019902,-6.17538739566531,3.13417605500228));
#5908=CARTESIAN_POINT('Ctrl Pts',(6.88237408148839,-6.2169021926909,3.15715697182391));
#5909=CARTESIAN_POINT('Ctrl Pts',(6.89697744222372,-6.23823300006139,3.17155768103299));
#5910=CARTESIAN_POINT('Ctrl Pts',(6.93296763252909,-6.29875591394082,3.22132213181236));
#5911=CARTESIAN_POINT('Ctrl Pts',(6.9474004570938,-6.33805779261652,3.26878119899199));
#5912=CARTESIAN_POINT('Ctrl Pts',(6.96319194510978,-6.391162819218,3.3786038562345));
#5913=CARTESIAN_POINT('Ctrl Pts',(6.9654030511288,-6.405,3.44082671433706));
#5914=CARTESIAN_POINT('Ctrl Pts',(6.9654030511288,-6.405,3.55917328566294));
#5915=CARTESIAN_POINT('Ctrl Pts',(6.96319194510978,-6.391162819218,3.6213961437655));
#5916=CARTESIAN_POINT('Ctrl Pts',(6.9474004570938,-6.33805779261652,3.73121880100801));
#5917=CARTESIAN_POINT('Ctrl Pts',(6.93296763252909,-6.29875591394082,3.77867786818764));
#5918=CARTESIAN_POINT('Ctrl Pts',(6.89697744222372,-6.23823300006139,3.82844231896701));
#5919=CARTESIAN_POINT('Ctrl Pts',(6.8823740814884,-6.2169021926909,3.84284302817609));
#5920=CARTESIAN_POINT('Ctrl Pts',(6.84782319019902,-6.17538739566531,3.86582394499772));
#5921=CARTESIAN_POINT('Ctrl Pts',(6.8278469830262,-6.1552757719279,3.87449161762901));
#5922=CARTESIAN_POINT('Ctrl Pts',(6.76795622589237,-6.10432382827604,3.8929902713498));
#5923=CARTESIAN_POINT('Ctrl Pts',(6.71846870594364,-6.07437258197005,3.89861533685297));
#5924=CARTESIAN_POINT('Ctrl Pts',(6.61134072173687,-6.03471454832095,3.90400536933732));
#5925=CARTESIAN_POINT('Ctrl Pts',(6.55372663006585,-6.025,3.90422765862815));
#5926=CARTESIAN_POINT('Ctrl Pts',(6.44627336993415,-6.025,3.90422765862815));
#5927=CARTESIAN_POINT('Ctrl Pts',(6.38865927826313,-6.03471454832095,3.90400536933732));
#5928=CARTESIAN_POINT('Ctrl Pts',(6.28153129405636,-6.07437258197005,3.89861533685297));
#5929=CARTESIAN_POINT('Ctrl Pts',(6.23204377410763,-6.10432382827604,3.8929902713498));
#5930=CARTESIAN_POINT('Ctrl Pts',(6.1721530169738,-6.1552757719279,3.87449161762901));
#5931=CARTESIAN_POINT('Ctrl Pts',(6.15217680980098,-6.17538739566531,3.86582394499772));
#5932=CARTESIAN_POINT('Ctrl Pts',(6.1176259185116,-6.2169021926909,3.84284302817609));
#5933=CARTESIAN_POINT('Ctrl Pts',(6.10302255777628,-6.23823300006139,3.82844231896701));
#5934=CARTESIAN_POINT('Ctrl Pts',(6.06703236747091,-6.29875591394082,3.77867786818764));
#5935=CARTESIAN_POINT('Ctrl Pts',(6.0525995429062,-6.33805779261652,3.73121880100801));
#5936=CARTESIAN_POINT('Ctrl Pts',(6.03680805489022,-6.391162819218,3.6213961437655));
#5937=CARTESIAN_POINT('Ctrl Pts',(6.0345969488712,-6.405,3.55917328566294));
#5938=CARTESIAN_POINT('Ctrl Pts',(6.0345969488712,-6.405,3.5));
#5939=CARTESIAN_POINT('Origin',(6.5,-6.5,1.8));
#5940=CARTESIAN_POINT('',(6.225,-6.5,1.8));
#5941=CARTESIAN_POINT('Origin',(6.5,-6.5,1.8));
#5942=CARTESIAN_POINT('Origin',(6.5,-6.5,0.9));
#5943=CARTESIAN_POINT('',(6.225,-6.5,1.));
#5944=CARTESIAN_POINT('Origin',(6.5,-6.5,1.));
#5945=CARTESIAN_POINT('',(6.225,-6.5,0.9));
#5946=CARTESIAN_POINT('Origin',(6.5,-4.2,0.9));
#5947=CARTESIAN_POINT('',(6.225,-4.2,1.));
#5948=CARTESIAN_POINT('Origin',(6.5,-4.2,1.));
#5949=CARTESIAN_POINT('',(6.225,-4.2,1.8));
#5950=CARTESIAN_POINT('',(6.225,-4.2,0.9));
#5951=CARTESIAN_POINT('Origin',(6.5,-4.2,1.8));
#5952=CARTESIAN_POINT('Origin',(5.9,-6.,3.5));
#5953=CARTESIAN_POINT('',(6.,-6.,3.905));
#5954=CARTESIAN_POINT('Origin',(6.,-6.,3.5));
#5955=CARTESIAN_POINT('',(7.,-6.,3.905));
#5956=CARTESIAN_POINT('',(5.9,-6.,3.905));
#5957=CARTESIAN_POINT('Origin',(7.,-6.,3.5));
#5958=CARTESIAN_POINT('Origin',(6.,-5.,4.5));
#5959=CARTESIAN_POINT('',(6.,-5.,4.5));
#5960=CARTESIAN_POINT('',(6.,-7.,4.5));
#5961=CARTESIAN_POINT('',(6.,-5.,4.5));
#5962=CARTESIAN_POINT('',(7.,-7.,4.5));
#5963=CARTESIAN_POINT('',(6.,-7.,4.5));
#5964=CARTESIAN_POINT('',(7.,-5.,4.5));
#5965=CARTESIAN_POINT('',(7.,-5.,4.5));
#5966=CARTESIAN_POINT('',(6.,-5.,4.5));
#5967=CARTESIAN_POINT('Origin',(6.,-5.,1.8));
#5968=CARTESIAN_POINT('',(6.,-5.,1.8));
#5969=CARTESIAN_POINT('',(6.,-5.,1.8));
#5970=CARTESIAN_POINT('',(7.,-5.,1.8));
#5971=CARTESIAN_POINT('',(7.,-5.,1.8));
#5972=CARTESIAN_POINT('',(6.,-5.,1.8));
#5973=CARTESIAN_POINT('Origin',(6.,-3.5,1.8));
#5974=CARTESIAN_POINT('',(6.,-3.5,1.8));
#5975=CARTESIAN_POINT('',(6.,-3.5,1.8));
#5976=CARTESIAN_POINT('',(7.,-3.5,1.8));
#5977=CARTESIAN_POINT('',(7.,-3.5,1.8));
#5978=CARTESIAN_POINT('',(6.,-3.5,1.8));
#5979=CARTESIAN_POINT('Origin',(6.,-3.5,1.));
#5980=CARTESIAN_POINT('',(6.,-3.5,1.));
#5981=CARTESIAN_POINT('',(6.,-3.5,1.));
#5982=CARTESIAN_POINT('',(7.,-3.5,1.));
#5983=CARTESIAN_POINT('',(7.,-3.5,1.));
#5984=CARTESIAN_POINT('',(6.,-3.5,1.));
#5985=CARTESIAN_POINT('Origin',(6.,-7.,1.));
#5986=CARTESIAN_POINT('',(6.,-7.,1.));
#5987=CARTESIAN_POINT('',(6.,-7.,1.));
#5988=CARTESIAN_POINT('',(7.,-7.,1.));
#5989=CARTESIAN_POINT('',(7.,-7.,1.));
#5990=CARTESIAN_POINT('',(6.,-7.,1.));
#5991=CARTESIAN_POINT('Origin',(6.,-7.,4.5));
#5992=CARTESIAN_POINT('',(6.,-7.,4.5));
#5993=CARTESIAN_POINT('',(7.,-7.,4.5));
#5994=CARTESIAN_POINT('Origin',(7.,-5.25,2.75));
#5995=CARTESIAN_POINT('Origin',(6.,-5.25,2.75));
#6591=UNCERTAINTY_MEASURE_WITH_UNIT(LENGTH_MEASURE(0.001),#6639,
'DISTANCE_ACCURACY_VALUE',
'Maximum model space distance between geometric entities at asserted c
onnectivities');
#6609=UNCERTAINTY_MEASURE_WITH_UNIT(LENGTH_MEASURE(0.001),#6639,
'DISTANCE_ACCURACY_VALUE',
'Maximum model space distance between geometric entities at asserted c
onnectivities');
#6620=(
GEOMETRIC_REPRESENTATION_CONTEXT(3)
GLOBAL_UNCERTAINTY_ASSIGNED_CONTEXT((#6591))
GLOBAL_UNIT_ASSIGNED_CONTEXT((#6639,#6641,#6642))
REPRESENTATION_CONTEXT('','3D')
);
#6638=(
GEOMETRIC_REPRESENTATION_CONTEXT(3)
GLOBAL_UNCERTAINTY_ASSIGNED_CONTEXT((#6609))
GLOBAL_UNIT_ASSIGNED_CONTEXT((#6639,#6641,#6642))
REPRESENTATION_CONTEXT('','3D')
);
#6639=(
LENGTH_UNIT()
NAMED_UNIT(*)
SI_UNIT(.CENTI.,.METRE.)
);
#6641=(
NAMED_UNIT(*)
PLANE_ANGLE_UNIT()
SI_UNIT($,.RADIAN.)
);
#6642=(
NAMED_UNIT(*)
SI_UNIT($,.STERADIAN.)
SOLID_ANGLE_UNIT()
);
#6653=SHAPE_DEFINITION_REPRESENTATION(#6681,#6747);
#6681=PRODUCT_DEFINITION_SHAPE('',$,#6776);
#6747=SHAPE_REPRESENTATION('',(#4025),#6620);
#6765=PRODUCT_DEFINITION_CONTEXT('part definition',#6851,'design');
#6776=PRODUCT_DEFINITION('Hinge lug (1)','Hinge lug (1)',#6804,#6765);
#6804=PRODUCT_DEFINITION_FORMATION('',$,#6863);
#6851=APPLICATION_CONTEXT(
'Core Data for Automotive Mechanical Design Process');
#6852=PRODUCT_CONTEXT('part definition',#6851,'mechanical');
#6863=PRODUCT('Hinge lug (1)','Hinge lug (1)','Hinge lug (1)',(#6852));
#6951=COLOUR_RGB('Off White',0.89,0.88,0.83);
#6952=FILL_AREA_STYLE_COLOUR('',#6951);
#6953=FILL_AREA_STYLE('',(#6952));
#6954=SURFACE_STYLE_FILL_AREA(#6953);
#6955=SURFACE_SIDE_STYLE('',(#6954));
#6956=SURFACE_STYLE_USAGE(.BOTH.,#6955);
#6957=PRESENTATION_STYLE_ASSIGNMENT((#6956));
ENDSEC;
END-ISO-10303-21;
